ISO-10303-21;
HEADER;
/* Generated by software containing ST-Developer
 * from STEP Tools, Inc. (www.steptools.com) 
 */

FILE_DESCRIPTION(
/* description */ ('PAT-091'),
/* implementation_level */ '2;1');

FILE_NAME(
/* name */ 'Axle end keeper (5).step',
/* time_stamp */ '2026-10-27T15:34:44-07:00',
/* author */ (''),
/* organization */ (''),
/* preprocessor_version */ 'ST-DEVELOPER v20.2',
/* originating_system */ 'Autodesk Translation Framework v15.17.0.0',
/* authorisation */ '');

FILE_SCHEMA (('AUTOMOTIVE_DESIGN { 1 0 10303 214 3 1 1 }'));
ENDSEC;

DATA;
#10=MECHANICAL_DESIGN_GEOMETRIC_PRESENTATION_REPRESENTATION('',(#1008),#25100);
#788=SHAPE_REPRESENTATION_RELATIONSHIP('SRR','None',#25551,#898);
#898=ADVANCED_BREP_SHAPE_REPRESENTATION('',(#1130),#25021);
#1008=STYLED_ITEM('',(#26191),#1130);
#1130=MANIFOLD_SOLID_BREP('Body1',#13287);
#1422=FACE_BOUND('',#3407,.T.);
#1423=FACE_BOUND('',#3409,.T.);
#1813=PLANE('',#15230);
#1814=PLANE('',#15231);
#2379=FACE_OUTER_BOUND('',#3404,.T.);
#2380=FACE_OUTER_BOUND('',#3405,.T.);
#2381=FACE_OUTER_BOUND('',#3406,.T.);
#2382=FACE_OUTER_BOUND('',#3408,.T.);
#3404=EDGE_LOOP('',(#10284,#10285,#10286,#10287));
#3405=EDGE_LOOP('',(#10288,#10289,#10290,#10291));
#3406=EDGE_LOOP('',(#10292));
#3407=EDGE_LOOP('',(#10293));
#3408=EDGE_LOOP('',(#10294));
#3409=EDGE_LOOP('',(#10295));
#4497=LINE('',#22453,#5237);
#4498=LINE('',#22459,#5238);
#5237=VECTOR('',#18123,0.225000000000001);
#5238=VECTOR('',#18130,1.);
#5885=CIRCLE('',#15225,0.225000000000001);
#5886=CIRCLE('',#15226,0.225000000000001);
#5887=CIRCLE('',#15228,1.);
#5888=CIRCLE('',#15229,1.);
#6818=VERTEX_POINT('',#22450);
#6819=VERTEX_POINT('',#22452);
#6820=VERTEX_POINT('',#22456);
#6821=VERTEX_POINT('',#22458);
#8077=EDGE_CURVE('',#6818,#6818,#5885,.T.);
#8078=EDGE_CURVE('',#6818,#6819,#4497,.T.);
#8079=EDGE_CURVE('',#6819,#6819,#5886,.T.);
#8080=EDGE_CURVE('',#6820,#6820,#5887,.T.);
#8081=EDGE_CURVE('',#6820,#6821,#4498,.T.);
#8082=EDGE_CURVE('',#6821,#6821,#5888,.T.);
#10284=ORIENTED_EDGE('',*,*,#8077,.F.);
#10285=ORIENTED_EDGE('',*,*,#8078,.T.);
#10286=ORIENTED_EDGE('',*,*,#8079,.T.);
#10287=ORIENTED_EDGE('',*,*,#8078,.F.);
#10288=ORIENTED_EDGE('',*,*,#8080,.F.);
#10289=ORIENTED_EDGE('',*,*,#8081,.T.);
#10290=ORIENTED_EDGE('',*,*,#8082,.T.);
#10291=ORIENTED_EDGE('',*,*,#8081,.F.);
#10292=ORIENTED_EDGE('',*,*,#8080,.T.);
#10293=ORIENTED_EDGE('',*,*,#8077,.T.);
#10294=ORIENTED_EDGE('',*,*,#8082,.F.);
#10295=ORIENTED_EDGE('',*,*,#8079,.F.);
#12210=CYLINDRICAL_SURFACE('',#15224,0.225000000000001);
#12211=CYLINDRICAL_SURFACE('',#15227,1.);
#12746=ADVANCED_FACE('',(#2379),#12210,.F.);
#12747=ADVANCED_FACE('',(#2380),#12211,.T.);
#12748=ADVANCED_FACE('',(#2381,#1422),#1813,.T.);
#12749=ADVANCED_FACE('',(#2382,#1423),#1814,.F.);
#13287=CLOSED_SHELL('',(#12746,#12747,#12748,#12749));
#15223=AXIS2_PLACEMENT_3D('',#22448,#18117,#18118);
#15224=AXIS2_PLACEMENT_3D('',#22449,#18119,#18120);
#15225=AXIS2_PLACEMENT_3D('',#22451,#18121,#18122);
#15226=AXIS2_PLACEMENT_3D('',#22454,#18124,#18125);
#15227=AXIS2_PLACEMENT_3D('',#22455,#18126,#18127);
#15228=AXIS2_PLACEMENT_3D('',#22457,#18128,#18129);
#15229=AXIS2_PLACEMENT_3D('',#22460,#18131,#18132);
#15230=AXIS2_PLACEMENT_3D('',#22461,#18133,#18134);
#15231=AXIS2_PLACEMENT_3D('',#22462,#18135,#18136);
#18117=DIRECTION('axis',(0.,0.,1.));
#18118=DIRECTION('refdir',(1.,0.,0.));
#18119=DIRECTION('center_axis',(0.,1.,0.));
#18120=DIRECTION('ref_axis',(1.,0.,0.));
#18121=DIRECTION('center_axis',(0.,-1.,0.));
#18122=DIRECTION('ref_axis',(1.,0.,0.));
#18123=DIRECTION('',(0.,-1.,0.));
#18124=DIRECTION('center_axis',(0.,-1.,0.));
#18125=DIRECTION('ref_axis',(1.,0.,0.));
#18126=DIRECTION('center_axis',(0.,1.,0.));
#18127=DIRECTION('ref_axis',(1.,0.,0.));
#18128=DIRECTION('center_axis',(0.,1.,0.));
#18129=DIRECTION('ref_axis',(1.,0.,0.));
#18130=DIRECTION('',(0.,-1.,0.));
#18131=DIRECTION('center_axis',(0.,1.,0.));
#18132=DIRECTION('ref_axis',(1.,0.,0.));
#18133=DIRECTION('center_axis',(0.,1.,0.));
#18134=DIRECTION('ref_axis',(1.,0.,0.));
#18135=DIRECTION('center_axis',(0.,1.,0.));
#18136=DIRECTION('ref_axis',(1.,0.,0.));
#22448=CARTESIAN_POINT('',(0.,0.,0.));
#22449=CARTESIAN_POINT('Origin',(38.7298334620742,8.5,3.));
#22450=CARTESIAN_POINT('',(38.5048334620742,8.7,3.));
#22451=CARTESIAN_POINT('Origin',(38.7298334620742,8.7,3.));
#22452=CARTESIAN_POINT('',(38.5048334620742,8.5,3.));
#22453=CARTESIAN_POINT('',(38.5048334620742,8.5,3.));
#22454=CARTESIAN_POINT('Origin',(38.7298334620742,8.5,3.));
#22455=CARTESIAN_POINT('Origin',(38.7298334620742,8.5,3.));
#22456=CARTESIAN_POINT('',(37.7298334620742,8.7,3.));
#22457=CARTESIAN_POINT('Origin',(38.7298334620742,8.7,3.));
#22458=CARTESIAN_POINT('',(37.7298334620742,8.5,3.));
#22459=CARTESIAN_POINT('',(37.7298334620742,8.5,3.));
#22460=CARTESIAN_POINT('Origin',(38.7298334620742,8.5,3.));
#22461=CARTESIAN_POINT('Origin',(38.7298334620742,8.7,3.));
#22462=CARTESIAN_POINT('Origin',(38.7298334620742,8.5,3.));
#24900=UNCERTAINTY_MEASURE_WITH_UNIT(LENGTH_MEASURE(0.001),#25101,
'DISTANCE_ACCURACY_VALUE',
'Maximum model space distance between geometric entities at asserted c
onnectivities');
#24979=UNCERTAINTY_MEASURE_WITH_UNIT(LENGTH_MEASURE(0.001),#25101,
'DISTANCE_ACCURACY_VALUE',
'Maximum model space distance between geometric entities at asserted c
onnectivities');
#25021=(
GEOMETRIC_REPRESENTATION_CONTEXT(3)
GLOBAL_UNCERTAINTY_ASSIGNED_CONTEXT((#24900))
GLOBAL_UNIT_ASSIGNED_CONTEXT((#25101,#25103,#25104))
REPRESENTATION_CONTEXT('','3D')
);
#25100=(
GEOMETRIC_REPRESENTATION_CONTEXT(3)
GLOBAL_UNCERTAINTY_ASSIGNED_CONTEXT((#24979))
GLOBAL_UNIT_ASSIGNED_CONTEXT((#25101,#25103,#25104))
REPRESENTATION_CONTEXT('','3D')
);
#25101=(
LENGTH_UNIT()
NAMED_UNIT(*)
SI_UNIT(.CENTI.,.METRE.)
);
#25103=(
NAMED_UNIT(*)
PLANE_ANGLE_UNIT()
SI_UNIT($,.RADIAN.)
);
#25104=(
NAMED_UNIT(*)
SI_UNIT($,.STERADIAN.)
SOLID_ANGLE_UNIT()
);
#25146=SHAPE_DEFINITION_REPRESENTATION(#25266,#25551);
#25266=PRODUCT_DEFINITION_SHAPE('',$,#25672);
#25551=SHAPE_REPRESENTATION('',(#15223),#25021);
#25630=PRODUCT_DEFINITION_CONTEXT('part definition',#25992,'design');
#25672=PRODUCT_DEFINITION('Axle end keeper (5)','Axle end keeper (5)',#25792,
#25630);
#25792=PRODUCT_DEFINITION_FORMATION('',$,#26035);
#25992=APPLICATION_CONTEXT(
'Core Data for Automotive Mechanical Design Process');
#25993=PRODUCT_CONTEXT('part definition',#25992,'mechanical');
#26035=PRODUCT('Axle end keeper (5)','Axle end keeper (5)',
'Axle end keeper (5)',(#25993));
#26185=COLOUR_RGB('Grey',0.48,0.52,0.57);
#26186=FILL_AREA_STYLE_COLOUR('',#26185);
#26187=FILL_AREA_STYLE('',(#26186));
#26188=SURFACE_STYLE_FILL_AREA(#26187);
#26189=SURFACE_SIDE_STYLE('',(#26188));
#26190=SURFACE_STYLE_USAGE(.BOTH.,#26189);
#26191=PRESENTATION_STYLE_ASSIGNMENT((#26190));
ENDSEC;
END-ISO-10303-21;
